ISO-10303-21;
HEADER;
/* Generated by software containing ST-Developer
 * from STEP Tools, Inc. (www.steptools.com) 
 */

FILE_DESCRIPTION(
/* description */ ('Caster wheel assembly'),
/* implementation_level */ '2;1');

FILE_NAME(
/* name */ 'Inner race spacer (1).step',
/* time_stamp */ '2026-10-28T03:23:56-07:00',
/* author */ (''),
/* organization */ (''),
/* preprocessor_version */ 'ST-DEVELOPER v20.2',
/* originating_system */ 'Autodesk Translation Framework v15.17.0.0',
/* authorisation */ '');

FILE_SCHEMA (('AUTOMOTIVE_DESIGN { 1 0 10303 214 3 1 1 }'));
ENDSEC;

DATA;
#10=MECHANICAL_DESIGN_GEOMETRIC_PRESENTATION_REPRESENTATION('',(#233),#5385);
#189=SHAPE_REPRESENTATION_RELATIONSHIP('SRR','None',#5485,#211);
#211=ADVANCED_BREP_SHAPE_REPRESENTATION('',(#263),#5372);
#233=STYLED_ITEM('',(#5672),#263);
#263=MANIFOLD_SOLID_BREP('Body1',#2660);
#311=FACE_BOUND('',#699,.T.);
#312=FACE_BOUND('',#701,.T.);
#381=PLANE('',#3082);
#382=PLANE('',#3083);
#498=FACE_OUTER_BOUND('',#696,.T.);
#499=FACE_OUTER_BOUND('',#697,.T.);
#500=FACE_OUTER_BOUND('',#698,.T.);
#501=FACE_OUTER_BOUND('',#700,.T.);
#696=EDGE_LOOP('',(#2084,#2085,#2086,#2087));
#697=EDGE_LOOP('',(#2088,#2089,#2090,#2091));
#698=EDGE_LOOP('',(#2092));
#699=EDGE_LOOP('',(#2093));
#700=EDGE_LOOP('',(#2094));
#701=EDGE_LOOP('',(#2095));
#892=LINE('',#4576,#1026);
#893=LINE('',#4582,#1027);
#1026=VECTOR('',#3697,0.505);
#1027=VECTOR('',#3704,0.7);
#1133=CIRCLE('',#3077,0.505);
#1134=CIRCLE('',#3078,0.505);
#1135=CIRCLE('',#3080,0.7);
#1136=CIRCLE('',#3081,0.7);
#1336=VERTEX_POINT('',#4573);
#1337=VERTEX_POINT('',#4575);
#1338=VERTEX_POINT('',#4579);
#1339=VERTEX_POINT('',#4581);
#1610=EDGE_CURVE('',#1336,#1336,#1133,.T.);
#1611=EDGE_CURVE('',#1336,#1337,#892,.T.);
#1612=EDGE_CURVE('',#1337,#1337,#1134,.T.);
#1613=EDGE_CURVE('',#1338,#1338,#1135,.T.);
#1614=EDGE_CURVE('',#1338,#1339,#893,.T.);
#1615=EDGE_CURVE('',#1339,#1339,#1136,.T.);
#2084=ORIENTED_EDGE('',*,*,#1610,.F.);
#2085=ORIENTED_EDGE('',*,*,#1611,.T.);
#2086=ORIENTED_EDGE('',*,*,#1612,.T.);
#2087=ORIENTED_EDGE('',*,*,#1611,.F.);
#2088=ORIENTED_EDGE('',*,*,#1613,.F.);
#2089=ORIENTED_EDGE('',*,*,#1614,.T.);
#2090=ORIENTED_EDGE('',*,*,#1615,.T.);
#2091=ORIENTED_EDGE('',*,*,#1614,.F.);
#2092=ORIENTED_EDGE('',*,*,#1613,.T.);
#2093=ORIENTED_EDGE('',*,*,#1610,.T.);
#2094=ORIENTED_EDGE('',*,*,#1615,.F.);
#2095=ORIENTED_EDGE('',*,*,#1612,.F.);
#2455=CYLINDRICAL_SURFACE('',#3076,0.505);
#2456=CYLINDRICAL_SURFACE('',#3079,0.7);
#2558=ADVANCED_FACE('',(#498),#2455,.F.);
#2559=ADVANCED_FACE('',(#499),#2456,.T.);
#2560=ADVANCED_FACE('',(#500,#311),#381,.T.);
#2561=ADVANCED_FACE('',(#501,#312),#382,.F.);
#2660=CLOSED_SHELL('',(#2558,#2559,#2560,#2561));
#3075=AXIS2_PLACEMENT_3D('',#4571,#3691,#3692);
#3076=AXIS2_PLACEMENT_3D('',#4572,#3693,#3694);
#3077=AXIS2_PLACEMENT_3D('',#4574,#3695,#3696);
#3078=AXIS2_PLACEMENT_3D('',#4577,#3698,#3699);
#3079=AXIS2_PLACEMENT_3D('',#4578,#3700,#3701);
#3080=AXIS2_PLACEMENT_3D('',#4580,#3702,#3703);
#3081=AXIS2_PLACEMENT_3D('',#4583,#3705,#3706);
#3082=AXIS2_PLACEMENT_3D('',#4584,#3707,#3708);
#3083=AXIS2_PLACEMENT_3D('',#4585,#3709,#3710);
#3691=DIRECTION('axis',(0.,0.,1.));
#3692=DIRECTION('refdir',(1.,0.,0.));
#3693=DIRECTION('center_axis',(0.,1.,0.));
#3694=DIRECTION('ref_axis',(1.,0.,0.));
#3695=DIRECTION('center_axis',(0.,-1.,0.));
#3696=DIRECTION('ref_axis',(1.,0.,0.));
#3697=DIRECTION('',(0.,-1.,0.));
#3698=DIRECTION('center_axis',(0.,-1.,0.));
#3699=DIRECTION('ref_axis',(1.,0.,0.));
#3700=DIRECTION('center_axis',(0.,1.,0.));
#3701=DIRECTION('ref_axis',(1.,0.,0.));
#3702=DIRECTION('center_axis',(0.,1.,0.));
#3703=DIRECTION('ref_axis',(1.,0.,0.));
#3704=DIRECTION('',(0.,-1.,0.));
#3705=DIRECTION('center_axis',(0.,1.,0.));
#3706=DIRECTION('ref_axis',(1.,0.,0.));
#3707=DIRECTION('center_axis',(0.,1.,0.));
#3708=DIRECTION('ref_axis',(1.,0.,0.));
#3709=DIRECTION('center_axis',(0.,1.,0.));
#3710=DIRECTION('ref_axis',(1.,0.,0.));
#4571=CARTESIAN_POINT('',(0.,0.,0.));
#4572=CARTESIAN_POINT('Origin',(0.,1.05,4.));
#4573=CARTESIAN_POINT('',(-0.505,1.8,4.));
#4574=CARTESIAN_POINT('Origin',(0.,1.8,4.));
#4575=CARTESIAN_POINT('',(-0.505,1.05,4.));
#4576=CARTESIAN_POINT('',(-0.505,1.05,4.));
#4577=CARTESIAN_POINT('Origin',(0.,1.05,4.));
#4578=CARTESIAN_POINT('Origin',(0.,1.05,4.));
#4579=CARTESIAN_POINT('',(-0.7,1.8,4.));
#4580=CARTESIAN_POINT('Origin',(0.,1.8,4.));
#4581=CARTESIAN_POINT('',(-0.7,1.05,4.));
#4582=CARTESIAN_POINT('',(-0.7,1.05,4.));
#4583=CARTESIAN_POINT('Origin',(0.,1.05,4.));
#4584=CARTESIAN_POINT('Origin',(0.,1.8,4.));
#4585=CARTESIAN_POINT('Origin',(0.,1.05,4.));
#5344=UNCERTAINTY_MEASURE_WITH_UNIT(LENGTH_MEASURE(0.001),#5386,
'DISTANCE_ACCURACY_VALUE',
'Maximum model space distance between geometric entities at asserted c
onnectivities');
#5357=UNCERTAINTY_MEASURE_WITH_UNIT(LENGTH_MEASURE(0.001),#5386,
'DISTANCE_ACCURACY_VALUE',
'Maximum model space distance between geometric entities at asserted c
onnectivities');
#5372=(
GEOMETRIC_REPRESENTATION_CONTEXT(3)
GLOBAL_UNCERTAINTY_ASSIGNED_CONTEXT((#5344))
GLOBAL_UNIT_ASSIGNED_CONTEXT((#5386,#5388,#5389))
REPRESENTATION_CONTEXT('','3D')
);
#5385=(
GEOMETRIC_REPRESENTATION_CONTEXT(3)
GLOBAL_UNCERTAINTY_ASSIGNED_CONTEXT((#5357))
GLOBAL_UNIT_ASSIGNED_CONTEXT((#5386,#5388,#5389))
REPRESENTATION_CONTEXT('','3D')
);
#5386=(
LENGTH_UNIT()
NAMED_UNIT(*)
SI_UNIT(.CENTI.,.METRE.)
);
#5388=(
NAMED_UNIT(*)
PLANE_ANGLE_UNIT()
SI_UNIT($,.RADIAN.)
);
#5389=(
NAMED_UNIT(*)
SI_UNIT($,.STERADIAN.)
SOLID_ANGLE_UNIT()
);
#5404=SHAPE_DEFINITION_REPRESENTATION(#5436,#5485);
#5436=PRODUCT_DEFINITION_SHAPE('',$,#5513);
#5485=SHAPE_REPRESENTATION('',(#3075),#5372);
#5498=PRODUCT_DEFINITION_CONTEXT('part definition',#5581,'design');
#5513=PRODUCT_DEFINITION('Inner race spacer (1)','Inner race spacer (1)',
#5540,#5498);
#5540=PRODUCT_DEFINITION_FORMATION('',$,#5597);
#5581=APPLICATION_CONTEXT(
'Core Data for Automotive Mechanical Design Process');
#5582=PRODUCT_CONTEXT('part definition',#5581,'mechanical');
#5597=PRODUCT('Inner race spacer (1)','Inner race spacer (1)',
'Inner race spacer (1)',(#5582));
#5666=COLOUR_RGB('Grey',0.48,0.52,0.57);
#5667=FILL_AREA_STYLE_COLOUR('',#5666);
#5668=FILL_AREA_STYLE('',(#5667));
#5669=SURFACE_STYLE_FILL_AREA(#5668);
#5670=SURFACE_SIDE_STYLE('',(#5669));
#5671=SURFACE_STYLE_USAGE(.BOTH.,#5670);
#5672=PRESENTATION_STYLE_ASSIGNMENT((#5671));
ENDSEC;
END-ISO-10303-21;
